ISO-10303-21;
HEADER;
/* Generated by software containing ST-Developer
 * from STEP Tools, Inc. (www.steptools.com) 
 */

FILE_DESCRIPTION(
/* description */ ('PAT-096'),
/* implementation_level */ '2;1');

FILE_NAME(
/* name */ 'M4x10 Cap Screw.step',
/* time_stamp */ '2026-10-29T17:03:14-07:00',
/* author */ (''),
/* organization */ (''),
/* preprocessor_version */ 'ST-DEVELOPER v20.2',
/* originating_system */ 'Autodesk Translation Framework v15.17.0.0',
/* authorisation */ '');

FILE_SCHEMA (('AUTOMOTIVE_DESIGN { 1 0 10303 214 3 1 1 }'));
ENDSEC;

DATA;
#10=MECHANICAL_DESIGN_GEOMETRIC_PRESENTATION_REPRESENTATION('',(#436),#10650);
#327=CONICAL_SURFACE('',#6607,0.325,0.785398163397448);
#328=CONICAL_SURFACE('',#6611,0.335,0.785398163397448);
#329=CONICAL_SURFACE('',#6615,0.21,0.463647609000806);
#332=ORIENTED_CLOSED_SHELL('',*,#5571,.F.);
#335=BREP_WITH_VOIDS('Body1',#5572,(#332));
#366=SHAPE_REPRESENTATION_RELATIONSHIP('SRR','None',#10831,#397);
#397=ADVANCED_BREP_SHAPE_REPRESENTATION('',(#335),#10649);
#436=STYLED_ITEM('',(#11071),#335);
#611=FACE_BOUND('',#1598,.T.);
#779=PLANE('',#6595);
#780=PLANE('',#6596);
#781=PLANE('',#6597);
#782=PLANE('',#6598);
#783=PLANE('',#6599);
#784=PLANE('',#6600);
#785=PLANE('',#6601);
#786=PLANE('',#6602);
#787=PLANE('',#6603);
#788=PLANE('',#6605);
#789=PLANE('',#6613);
#1110=FACE_OUTER_BOUND('',#1584,.T.);
#1111=FACE_OUTER_BOUND('',#1585,.T.);
#1112=FACE_OUTER_BOUND('',#1586,.T.);
#1113=FACE_OUTER_BOUND('',#1587,.T.);
#1114=FACE_OUTER_BOUND('',#1588,.T.);
#1115=FACE_OUTER_BOUND('',#1589,.T.);
#1116=FACE_OUTER_BOUND('',#1590,.T.);
#1117=FACE_OUTER_BOUND('',#1591,.T.);
#1118=FACE_OUTER_BOUND('',#1592,.T.);
#1119=FACE_OUTER_BOUND('',#1593,.T.);
#1120=FACE_OUTER_BOUND('',#1594,.T.);
#1121=FACE_OUTER_BOUND('',#1595,.T.);
#1122=FACE_OUTER_BOUND('',#1596,.T.);
#1123=FACE_OUTER_BOUND('',#1597,.T.);
#1124=FACE_OUTER_BOUND('',#1599,.T.);
#1125=FACE_OUTER_BOUND('',#1600,.T.);
#1584=EDGE_LOOP('',(#5013,#5014,#5015,#5016));
#1585=EDGE_LOOP('',(#5017,#5018,#5019,#5020));
#1586=EDGE_LOOP('',(#5021,#5022,#5023,#5024));
#1587=EDGE_LOOP('',(#5025,#5026,#5027,#5028));
#1588=EDGE_LOOP('',(#5029,#5030,#5031,#5032));
#1589=EDGE_LOOP('',(#5033,#5034,#5035,#5036));
#1590=EDGE_LOOP('',(#5037,#5038,#5039,#5040,#5041,#5042));
#1591=EDGE_LOOP('',(#5043,#5044,#5045,#5046,#5047,#5048));
#1592=EDGE_LOOP('',(#5049));
#1593=EDGE_LOOP('',(#5050));
#1594=EDGE_LOOP('',(#5051,#5052,#5053,#5054));
#1595=EDGE_LOOP('',(#5055,#5056,#5057,#5058));
#1596=EDGE_LOOP('',(#5059,#5060,#5061,#5062));
#1597=EDGE_LOOP('',(#5063));
#1598=EDGE_LOOP('',(#5064));
#1599=EDGE_LOOP('',(#5065,#5066,#5067,#5068));
#1600=EDGE_LOOP('',(#5069,#5070,#5071,#5072));
#1907=LINE('',#10458,#2236);
#1908=LINE('',#10460,#2237);
#1909=LINE('',#10462,#2238);
#1910=LINE('',#10463,#2239);
#1911=LINE('',#10466,#2240);
#1912=LINE('',#10468,#2241);
#1913=LINE('',#10469,#2242);
#1914=LINE('',#10472,#2243);
#1915=LINE('',#10474,#2244);
#1916=LINE('',#10475,#2245);
#1917=LINE('',#10478,#2246);
#1918=LINE('',#10480,#2247);
#1919=LINE('',#10481,#2248);
#1920=LINE('',#10484,#2249);
#1921=LINE('',#10486,#2250);
#1922=LINE('',#10487,#2251);
#1923=LINE('',#10489,#2252);
#1924=LINE('',#10490,#2253);
#1925=LINE('',#10502,#2254);
#1926=LINE('',#10506,#2255);
#1927=LINE('',#10510,#2256);
#1928=LINE('',#10517,#2257);
#1929=LINE('',#10519,#2258);
#2236=VECTOR('',#8339,1.);
#2237=VECTOR('',#8340,1.);
#2238=VECTOR('',#8341,1.);
#2239=VECTOR('',#8342,1.);
#2240=VECTOR('',#8345,1.);
#2241=VECTOR('',#8346,1.);
#2242=VECTOR('',#8347,1.);
#2243=VECTOR('',#8350,1.);
#2244=VECTOR('',#8351,1.);
#2245=VECTOR('',#8352,1.);
#2246=VECTOR('',#8355,1.);
#2247=VECTOR('',#8356,1.);
#2248=VECTOR('',#8357,1.);
#2249=VECTOR('',#8360,1.);
#2250=VECTOR('',#8361,1.);
#2251=VECTOR('',#8362,1.);
#2252=VECTOR('',#8365,1.);
#2253=VECTOR('',#8366,1.);
#2254=VECTOR('',#8383,0.325);
#2255=VECTOR('',#8388,0.35);
#2256=VECTOR('',#8393,0.335);
#2257=VECTOR('',#8402,0.21);
#2258=VECTOR('',#8405,0.2);
#2571=CIRCLE('',#6604,0.1954);
#2572=CIRCLE('',#6606,0.3);
#2573=CIRCLE('',#6608,0.35);
#2574=CIRCLE('',#6610,0.35);
#2575=CIRCLE('',#6612,0.32);
#2576=CIRCLE('',#6614,0.22);
#2577=CIRCLE('',#6616,0.1954);
#3017=VERTEX_POINT('',#10456);
#3018=VERTEX_POINT('',#10457);
#3019=VERTEX_POINT('',#10459);
#3020=VERTEX_POINT('',#10461);
#3021=VERTEX_POINT('',#10465);
#3022=VERTEX_POINT('',#10467);
#3023=VERTEX_POINT('',#10471);
#3024=VERTEX_POINT('',#10473);
#3025=VERTEX_POINT('',#10477);
#3026=VERTEX_POINT('',#10479);
#3027=VERTEX_POINT('',#10483);
#3028=VERTEX_POINT('',#10485);
#3029=VERTEX_POINT('',#10494);
#3030=VERTEX_POINT('',#10497);
#3031=VERTEX_POINT('',#10500);
#3032=VERTEX_POINT('',#10504);
#3033=VERTEX_POINT('',#10508);
#3034=VERTEX_POINT('',#10512);
#3035=VERTEX_POINT('',#10515);
#3685=EDGE_CURVE('',#3017,#3018,#1907,.T.);
#3686=EDGE_CURVE('',#3018,#3019,#1908,.T.);
#3687=EDGE_CURVE('',#3019,#3020,#1909,.T.);
#3688=EDGE_CURVE('',#3017,#3020,#1910,.T.);
#3689=EDGE_CURVE('',#3018,#3021,#1911,.T.);
#3690=EDGE_CURVE('',#3021,#3022,#1912,.T.);
#3691=EDGE_CURVE('',#3022,#3019,#1913,.T.);
#3692=EDGE_CURVE('',#3021,#3023,#1914,.T.);
#3693=EDGE_CURVE('',#3023,#3024,#1915,.T.);
#3694=EDGE_CURVE('',#3024,#3022,#1916,.T.);
#3695=EDGE_CURVE('',#3023,#3025,#1917,.T.);
#3696=EDGE_CURVE('',#3025,#3026,#1918,.T.);
#3697=EDGE_CURVE('',#3026,#3024,#1919,.T.);
#3698=EDGE_CURVE('',#3025,#3027,#1920,.T.);
#3699=EDGE_CURVE('',#3027,#3028,#1921,.T.);
#3700=EDGE_CURVE('',#3028,#3026,#1922,.T.);
#3701=EDGE_CURVE('',#3027,#3017,#1923,.T.);
#3702=EDGE_CURVE('',#3020,#3028,#1924,.T.);
#3703=EDGE_CURVE('',#3029,#3029,#2571,.T.);
#3704=EDGE_CURVE('',#3030,#3030,#2572,.T.);
#3705=EDGE_CURVE('',#3031,#3031,#2573,.T.);
#3706=EDGE_CURVE('',#3031,#3030,#1925,.T.);
#3707=EDGE_CURVE('',#3032,#3032,#2574,.T.);
#3708=EDGE_CURVE('',#3032,#3031,#1926,.T.);
#3709=EDGE_CURVE('',#3033,#3033,#2575,.T.);
#3710=EDGE_CURVE('',#3033,#3032,#1927,.T.);
#3711=EDGE_CURVE('',#3034,#3034,#2576,.T.);
#3712=EDGE_CURVE('',#3035,#3035,#2577,.F.);
#3713=EDGE_CURVE('',#3035,#3034,#1928,.T.);
#3714=EDGE_CURVE('',#3029,#3035,#1929,.T.);
#5013=ORIENTED_EDGE('',*,*,#3685,.T.);
#5014=ORIENTED_EDGE('',*,*,#3686,.T.);
#5015=ORIENTED_EDGE('',*,*,#3687,.T.);
#5016=ORIENTED_EDGE('',*,*,#3688,.F.);
#5017=ORIENTED_EDGE('',*,*,#3689,.T.);
#5018=ORIENTED_EDGE('',*,*,#3690,.T.);
#5019=ORIENTED_EDGE('',*,*,#3691,.T.);
#5020=ORIENTED_EDGE('',*,*,#3686,.F.);
#5021=ORIENTED_EDGE('',*,*,#3692,.T.);
#5022=ORIENTED_EDGE('',*,*,#3693,.T.);
#5023=ORIENTED_EDGE('',*,*,#3694,.T.);
#5024=ORIENTED_EDGE('',*,*,#3690,.F.);
#5025=ORIENTED_EDGE('',*,*,#3695,.T.);
#5026=ORIENTED_EDGE('',*,*,#3696,.T.);
#5027=ORIENTED_EDGE('',*,*,#3697,.T.);
#5028=ORIENTED_EDGE('',*,*,#3693,.F.);
#5029=ORIENTED_EDGE('',*,*,#3698,.T.);
#5030=ORIENTED_EDGE('',*,*,#3699,.T.);
#5031=ORIENTED_EDGE('',*,*,#3700,.T.);
#5032=ORIENTED_EDGE('',*,*,#3696,.F.);
#5033=ORIENTED_EDGE('',*,*,#3701,.T.);
#5034=ORIENTED_EDGE('',*,*,#3688,.T.);
#5035=ORIENTED_EDGE('',*,*,#3702,.T.);
#5036=ORIENTED_EDGE('',*,*,#3699,.F.);
#5037=ORIENTED_EDGE('',*,*,#3701,.F.);
#5038=ORIENTED_EDGE('',*,*,#3698,.F.);
#5039=ORIENTED_EDGE('',*,*,#3695,.F.);
#5040=ORIENTED_EDGE('',*,*,#3692,.F.);
#5041=ORIENTED_EDGE('',*,*,#3689,.F.);
#5042=ORIENTED_EDGE('',*,*,#3685,.F.);
#5043=ORIENTED_EDGE('',*,*,#3702,.F.);
#5044=ORIENTED_EDGE('',*,*,#3687,.F.);
#5045=ORIENTED_EDGE('',*,*,#3691,.F.);
#5046=ORIENTED_EDGE('',*,*,#3694,.F.);
#5047=ORIENTED_EDGE('',*,*,#3697,.F.);
#5048=ORIENTED_EDGE('',*,*,#3700,.F.);
#5049=ORIENTED_EDGE('',*,*,#3703,.F.);
#5050=ORIENTED_EDGE('',*,*,#3704,.F.);
#5051=ORIENTED_EDGE('',*,*,#3705,.F.);
#5052=ORIENTED_EDGE('',*,*,#3706,.T.);
#5053=ORIENTED_EDGE('',*,*,#3704,.T.);
#5054=ORIENTED_EDGE('',*,*,#3706,.F.);
#5055=ORIENTED_EDGE('',*,*,#3707,.F.);
#5056=ORIENTED_EDGE('',*,*,#3708,.T.);
#5057=ORIENTED_EDGE('',*,*,#3705,.T.);
#5058=ORIENTED_EDGE('',*,*,#3708,.F.);
#5059=ORIENTED_EDGE('',*,*,#3709,.F.);
#5060=ORIENTED_EDGE('',*,*,#3710,.T.);
#5061=ORIENTED_EDGE('',*,*,#3707,.T.);
#5062=ORIENTED_EDGE('',*,*,#3710,.F.);
#5063=ORIENTED_EDGE('',*,*,#3709,.T.);
#5064=ORIENTED_EDGE('',*,*,#3711,.F.);
#5065=ORIENTED_EDGE('',*,*,#3712,.F.);
#5066=ORIENTED_EDGE('',*,*,#3713,.T.);
#5067=ORIENTED_EDGE('',*,*,#3711,.T.);
#5068=ORIENTED_EDGE('',*,*,#3713,.F.);
#5069=ORIENTED_EDGE('',*,*,#3703,.T.);
#5070=ORIENTED_EDGE('',*,*,#3714,.T.);
#5071=ORIENTED_EDGE('',*,*,#3712,.T.);
#5072=ORIENTED_EDGE('',*,*,#3714,.F.);
#5193=CYLINDRICAL_SURFACE('',#6609,0.35);
#5194=CYLINDRICAL_SURFACE('',#6617,0.1954);
#5515=ADVANCED_FACE('',(#1110),#779,.F.);
#5516=ADVANCED_FACE('',(#1111),#780,.F.);
#5517=ADVANCED_FACE('',(#1112),#781,.F.);
#5518=ADVANCED_FACE('',(#1113),#782,.F.);
#5519=ADVANCED_FACE('',(#1114),#783,.F.);
#5520=ADVANCED_FACE('',(#1115),#784,.F.);
#5521=ADVANCED_FACE('',(#1116),#785,.F.);
#5522=ADVANCED_FACE('',(#1117),#786,.F.);
#5523=ADVANCED_FACE('',(#1118),#787,.F.);
#5524=ADVANCED_FACE('',(#1119),#788,.T.);
#5525=ADVANCED_FACE('',(#1120),#327,.T.);
#5526=ADVANCED_FACE('',(#1121),#5193,.T.);
#5527=ADVANCED_FACE('',(#1122),#328,.T.);
#5528=ADVANCED_FACE('',(#1123,#611),#789,.T.);
#5529=ADVANCED_FACE('',(#1124),#329,.T.);
#5530=ADVANCED_FACE('',(#1125),#5194,.T.);
#5571=CLOSED_SHELL('',(#5515,#5516,#5517,#5518,#5519,#5520,#5521,#5522));
#5572=CLOSED_SHELL('',(#5523,#5524,#5525,#5526,#5527,#5528,#5529,#5530));
#6594=AXIS2_PLACEMENT_3D('',#10454,#8335,#8336);
#6595=AXIS2_PLACEMENT_3D('',#10455,#8337,#8338);
#6596=AXIS2_PLACEMENT_3D('',#10464,#8343,#8344);
#6597=AXIS2_PLACEMENT_3D('',#10470,#8348,#8349);
#6598=AXIS2_PLACEMENT_3D('',#10476,#8353,#8354);
#6599=AXIS2_PLACEMENT_3D('',#10482,#8358,#8359);
#6600=AXIS2_PLACEMENT_3D('',#10488,#8363,#8364);
#6601=AXIS2_PLACEMENT_3D('',#10491,#8367,#8368);
#6602=AXIS2_PLACEMENT_3D('',#10492,#8369,#8370);
#6603=AXIS2_PLACEMENT_3D('',#10493,#8371,#8372);
#6604=AXIS2_PLACEMENT_3D('',#10495,#8373,#8374);
#6605=AXIS2_PLACEMENT_3D('',#10496,#8375,#8376);
#6606=AXIS2_PLACEMENT_3D('',#10498,#8377,#8378);
#6607=AXIS2_PLACEMENT_3D('',#10499,#8379,#8380);
#6608=AXIS2_PLACEMENT_3D('',#10501,#8381,#8382);
#6609=AXIS2_PLACEMENT_3D('',#10503,#8384,#8385);
#6610=AXIS2_PLACEMENT_3D('',#10505,#8386,#8387);
#6611=AXIS2_PLACEMENT_3D('',#10507,#8389,#8390);
#6612=AXIS2_PLACEMENT_3D('',#10509,#8391,#8392);
#6613=AXIS2_PLACEMENT_3D('',#10511,#8394,#8395);
#6614=AXIS2_PLACEMENT_3D('',#10513,#8396,#8397);
#6615=AXIS2_PLACEMENT_3D('',#10514,#8398,#8399);
#6616=AXIS2_PLACEMENT_3D('',#10516,#8400,#8401);
#6617=AXIS2_PLACEMENT_3D('',#10518,#8403,#8404);
#8335=DIRECTION('axis',(0.,0.,1.));
#8336=DIRECTION('refdir',(1.,0.,0.));
#8337=DIRECTION('center_axis',(0.866025403784439,0.,-0.5));
#8338=DIRECTION('ref_axis',(0.5,0.,0.866025403784439));
#8339=DIRECTION('',(-0.5,0.,-0.866025403784439));
#8340=DIRECTION('',(0.,-1.,0.));
#8341=DIRECTION('',(0.5,0.,0.866025403784439));
#8342=DIRECTION('',(0.,-1.,0.));
#8343=DIRECTION('center_axis',(1.60246890531964E-16,0.,-1.));
#8344=DIRECTION('ref_axis',(1.,0.,1.60246890531964E-16));
#8345=DIRECTION('',(-1.,0.,-1.60246890531964E-16));
#8346=DIRECTION('',(0.,-1.,0.));
#8347=DIRECTION('',(1.,0.,1.60246890531964E-16));
#8348=DIRECTION('center_axis',(-0.866025403784439,0.,-0.5));
#8349=DIRECTION('ref_axis',(0.5,0.,-0.866025403784439));
#8350=DIRECTION('',(-0.5,0.,0.866025403784439));
#8351=DIRECTION('',(0.,-1.,0.));
#8352=DIRECTION('',(0.5,0.,-0.866025403784439));
#8353=DIRECTION('center_axis',(-0.866025403784439,0.,0.5));
#8354=DIRECTION('ref_axis',(-0.5,0.,-0.866025403784439));
#8355=DIRECTION('',(0.5,0.,0.866025403784439));
#8356=DIRECTION('',(0.,-1.,0.));
#8357=DIRECTION('',(-0.5,0.,-0.866025403784439));
#8358=DIRECTION('center_axis',(-1.60246890531964E-16,0.,1.));
#8359=DIRECTION('ref_axis',(-1.,0.,-1.60246890531964E-16));
#8360=DIRECTION('',(1.,0.,1.60246890531964E-16));
#8361=DIRECTION('',(0.,-1.,0.));
#8362=DIRECTION('',(-1.,0.,-1.60246890531964E-16));
#8363=DIRECTION('center_axis',(0.866025403784439,0.,0.5));
#8364=DIRECTION('ref_axis',(-0.5,0.,0.866025403784439));
#8365=DIRECTION('',(0.5,0.,-0.866025403784439));
#8366=DIRECTION('',(-0.5,0.,0.866025403784439));
#8367=DIRECTION('center_axis',(0.,1.,0.));
#8368=DIRECTION('ref_axis',(1.,0.,0.));
#8369=DIRECTION('center_axis',(0.,-1.,0.));
#8370=DIRECTION('ref_axis',(0.,0.,-1.));
#8371=DIRECTION('center_axis',(0.,1.,0.));
#8372=DIRECTION('ref_axis',(1.,0.,0.));
#8373=DIRECTION('center_axis',(0.,1.,0.));
#8374=DIRECTION('ref_axis',(1.,0.,0.));
#8375=DIRECTION('center_axis',(0.,1.,0.));
#8376=DIRECTION('ref_axis',(0.,0.,1.));
#8377=DIRECTION('center_axis',(0.,-1.,0.));
#8378=DIRECTION('ref_axis',(1.,0.,0.));
#8379=DIRECTION('center_axis',(0.,-1.,0.));
#8380=DIRECTION('ref_axis',(1.,0.,0.));
#8381=DIRECTION('center_axis',(0.,-1.,0.));
#8382=DIRECTION('ref_axis',(1.,0.,0.));
#8383=DIRECTION('',(0.707106781186547,0.707106781186548,8.65956056235493E-17));
#8384=DIRECTION('center_axis',(0.,-1.,0.));
#8385=DIRECTION('ref_axis',(1.,0.,0.));
#8386=DIRECTION('center_axis',(0.,-1.,0.));
#8387=DIRECTION('ref_axis',(1.,0.,0.));
#8388=DIRECTION('',(0.,1.,0.));
#8389=DIRECTION('center_axis',(0.,1.,0.));
#8390=DIRECTION('ref_axis',(1.,0.,0.));
#8391=DIRECTION('center_axis',(0.,-1.,0.));
#8392=DIRECTION('ref_axis',(1.,0.,0.));
#8393=DIRECTION('',(-0.707106781186547,0.707106781186548,-8.65956056235493E-17));
#8394=DIRECTION('center_axis',(0.,-1.,0.));
#8395=DIRECTION('ref_axis',(0.,0.,-1.));
#8396=DIRECTION('center_axis',(0.,-1.,0.));
#8397=DIRECTION('ref_axis',(1.,0.,0.));
#8398=DIRECTION('center_axis',(0.,1.,0.));
#8399=DIRECTION('ref_axis',(1.,0.,0.));
#8400=DIRECTION('center_axis',(0.,1.,0.));
#8401=DIRECTION('ref_axis',(1.,0.,0.));
#8402=DIRECTION('',(-0.447213595499958,0.894427190999916,-5.47678698264203E-17));
#8403=DIRECTION('center_axis',(0.,-1.,0.));
#8404=DIRECTION('ref_axis',(1.,0.,0.));
#8405=DIRECTION('',(0.,1.,0.));
#10454=CARTESIAN_POINT('',(0.,0.,0.));
#10455=CARTESIAN_POINT('Origin',(0.0866025403784439,-0.4,-0.15));
#10456=CARTESIAN_POINT('',(0.173205080756888,-0.4,0.));
#10457=CARTESIAN_POINT('',(0.0866025403784439,-0.4,-0.15));
#10458=CARTESIAN_POINT('',(0.173205080756888,-0.4,0.));
#10459=CARTESIAN_POINT('',(0.0866025403784439,-0.64,-0.15));
#10460=CARTESIAN_POINT('',(0.0866025403784439,-0.4,-0.15));
#10461=CARTESIAN_POINT('',(0.173205080756888,-0.64,0.));
#10462=CARTESIAN_POINT('',(0.173205080756888,-0.64,0.));
#10463=CARTESIAN_POINT('',(0.173205080756888,-0.4,0.));
#10464=CARTESIAN_POINT('Origin',(-0.0866025403784438,-0.4,-0.15));
#10465=CARTESIAN_POINT('',(-0.0866025403784438,-0.4,-0.15));
#10466=CARTESIAN_POINT('',(0.0866025403784439,-0.4,-0.15));
#10467=CARTESIAN_POINT('',(-0.0866025403784438,-0.64,-0.15));
#10468=CARTESIAN_POINT('',(-0.0866025403784438,-0.4,-0.15));
#10469=CARTESIAN_POINT('',(0.0866025403784439,-0.64,-0.15));
#10470=CARTESIAN_POINT('Origin',(-0.173205080756888,-0.4,-2.77555756156289E-17));
#10471=CARTESIAN_POINT('',(-0.173205080756888,-0.4,-2.12115047744981E-17));
#10472=CARTESIAN_POINT('',(-0.0866025403784438,-0.4,-0.15));
#10473=CARTESIAN_POINT('',(-0.173205080756888,-0.64,-2.77555756156289E-17));
#10474=CARTESIAN_POINT('',(-0.173205080756888,-0.4,-2.12115047744981E-17));
#10475=CARTESIAN_POINT('',(-0.0866025403784438,-0.64,-0.15));
#10476=CARTESIAN_POINT('Origin',(-0.0866025403784439,-0.4,0.15));
#10477=CARTESIAN_POINT('',(-0.0866025403784439,-0.4,0.15));
#10478=CARTESIAN_POINT('',(-0.173205080756888,-0.4,-2.12115047744981E-17));
#10479=CARTESIAN_POINT('',(-0.0866025403784439,-0.64,0.15));
#10480=CARTESIAN_POINT('',(-0.0866025403784439,-0.4,0.15));
#10481=CARTESIAN_POINT('',(-0.173205080756888,-0.64,-2.12115047744981E-17));
#10482=CARTESIAN_POINT('Origin',(0.0866025403784439,-0.4,0.15));
#10483=CARTESIAN_POINT('',(0.0866025403784439,-0.4,0.15));
#10484=CARTESIAN_POINT('',(-0.0866025403784439,-0.4,0.15));
#10485=CARTESIAN_POINT('',(0.0866025403784439,-0.64,0.15));
#10486=CARTESIAN_POINT('',(0.0866025403784439,-0.4,0.15));
#10487=CARTESIAN_POINT('',(-0.0866025403784439,-0.64,0.15));
#10488=CARTESIAN_POINT('Origin',(0.173205080756888,-0.4,0.));
#10489=CARTESIAN_POINT('',(0.0866025403784439,-0.4,0.15));
#10490=CARTESIAN_POINT('',(0.0866025403784439,-0.64,0.15));
#10491=CARTESIAN_POINT('Origin',(0.,-0.4,-2.77555756156289E-17));
#10492=CARTESIAN_POINT('Origin',(0.,-0.64,-2.77555756156289E-17));
#10493=CARTESIAN_POINT('Origin',(0.,-1.,0.));
#10494=CARTESIAN_POINT('',(-0.1954,-1.,2.39295984553393E-17));
#10495=CARTESIAN_POINT('Origin',(0.,-1.,0.));
#10496=CARTESIAN_POINT('Origin',(0.3,0.4,0.));
#10497=CARTESIAN_POINT('',(-0.3,0.4,-3.67394039744206E-17));
#10498=CARTESIAN_POINT('Origin',(0.,0.4,0.));
#10499=CARTESIAN_POINT('Origin',(0.,0.375,0.));
#10500=CARTESIAN_POINT('',(-0.35,0.35,-4.28626379701573E-17));
#10501=CARTESIAN_POINT('Origin',(0.,0.35,0.));
#10502=CARTESIAN_POINT('',(-0.325,0.375,-3.9801020972289E-17));
#10503=CARTESIAN_POINT('Origin',(0.,0.19,0.));
#10504=CARTESIAN_POINT('',(-0.35,0.03,-4.28626379701574E-17));
#10505=CARTESIAN_POINT('Origin',(0.,0.03,0.));
#10506=CARTESIAN_POINT('',(-0.35,0.19,-4.28626379701574E-17));
#10507=CARTESIAN_POINT('Origin',(0.,0.0149999999999999,0.));
#10508=CARTESIAN_POINT('',(-0.32,-3.29597460435593E-17,-3.91886975727153E-17));
#10509=CARTESIAN_POINT('Origin',(0.,0.,0.));
#10510=CARTESIAN_POINT('',(-0.335,0.0149999999999999,-4.10256677714363E-17));
#10511=CARTESIAN_POINT('Origin',(0.22,0.,0.));
#10512=CARTESIAN_POINT('',(-0.22,-6.93889390390723E-18,-2.69422295812418E-17));
#10513=CARTESIAN_POINT('Origin',(0.,0.,0.));
#10514=CARTESIAN_POINT('Origin',(0.,-0.02,0.));
#10515=CARTESIAN_POINT('',(-0.1954,-0.0492,2.39295984553393E-17));
#10516=CARTESIAN_POINT('Origin',(0.,-0.0492,0.));
#10517=CARTESIAN_POINT('',(-0.21,-0.02,-2.57175827820944E-17));
#10518=CARTESIAN_POINT('Origin',(0.,-0.8,0.));
#10519=CARTESIAN_POINT('',(-0.1954,-0.8,-2.39295984553393E-17));
#10610=UNCERTAINTY_MEASURE_WITH_UNIT(LENGTH_MEASURE(0.001),#10651,
'DISTANCE_ACCURACY_VALUE',
'Maximum model space distance between geometric entities at asserted c
onnectivities');
#10611=UNCERTAINTY_MEASURE_WITH_UNIT(LENGTH_MEASURE(0.001),#10651,
'DISTANCE_ACCURACY_VALUE',
'Maximum model space distance between geometric entities at asserted c
onnectivities');
#10649=(
GEOMETRIC_REPRESENTATION_CONTEXT(3)
GLOBAL_UNCERTAINTY_ASSIGNED_CONTEXT((#10610))
GLOBAL_UNIT_ASSIGNED_CONTEXT((#10651,#10653,#10654))
REPRESENTATION_CONTEXT('','3D')
);
#10650=(
GEOMETRIC_REPRESENTATION_CONTEXT(3)
GLOBAL_UNCERTAINTY_ASSIGNED_CONTEXT((#10611))
GLOBAL_UNIT_ASSIGNED_CONTEXT((#10651,#10653,#10654))
REPRESENTATION_CONTEXT('','3D')
);
#10651=(
LENGTH_UNIT()
NAMED_UNIT(*)
SI_UNIT(.CENTI.,.METRE.)
);
#10653=(
NAMED_UNIT(*)
PLANE_ANGLE_UNIT()
SI_UNIT($,.RADIAN.)
);
#10654=(
NAMED_UNIT(*)
SI_UNIT($,.STERADIAN.)
SOLID_ANGLE_UNIT()
);
#10692=SHAPE_DEFINITION_REPRESENTATION(#10740,#10831);
#10740=PRODUCT_DEFINITION_SHAPE('',$,#10870);
#10831=SHAPE_REPRESENTATION('',(#6594),#10649);
#10832=PRODUCT_DEFINITION_CONTEXT('part definition',#10948,'design');
#10870=PRODUCT_DEFINITION('M4x10 Cap Screw','M4x10 Cap Screw',#10908,#10832);
#10908=PRODUCT_DEFINITION_FORMATION('',$,#10987);
#10948=APPLICATION_CONTEXT(
'Core Data for Automotive Mechanical Design Process');
#10949=PRODUCT_CONTEXT('part definition',#10948,'mechanical');
#10987=PRODUCT('M4x10 Cap Screw','M4x10 Cap Screw','M4x10 Cap Screw',(#10949));
#11065=COLOUR_RGB('Black',0.12,0.14,0.17);
#11066=FILL_AREA_STYLE_COLOUR('',#11065);
#11067=FILL_AREA_STYLE('',(#11066));
#11068=SURFACE_STYLE_FILL_AREA(#11067);
#11069=SURFACE_SIDE_STYLE('',(#11068));
#11070=SURFACE_STYLE_USAGE(.BOTH.,#11069);
#11071=PRESENTATION_STYLE_ASSIGNMENT((#11070));
ENDSEC;
END-ISO-10303-21;
